ISO-10303-21;
HEADER;
/* Generated by software containing ST-Developer
 * from STEP Tools, Inc. (www.steptools.com) 
 */
/* OPTION: using custom renumber hook */

FILE_DESCRIPTION(
/* description */ ('STEP AP242 Edition 2', 'CAx-IF Rec.Pracs.---Representation and Presentation of Product Manufa
cturing Information (PMI)---4.0---2014-10-13', 'CAx-IF Rec.Pracs.---3D Tessellated Geometry---0.4---2014-09-14', '2;1', 'CAx-IF Rec.Pracs.---User Defined Attributes---1.5---2016-08-15'),
/* implementation_level */ '2;1');

FILE_NAME(
/* name */ 'Neck_flat_seal.step',
/* time_stamp */ '2026-10-08T12:15:07Z',
/* author */ (''),
/* organization */ (''),
/* preprocessor_version */ 'ST-DEVELOPER v20',
/* originating_system */ 'ONSHAPE BY PTC INC, 1.221',
/* authorisation */ '  ');

FILE_SCHEMA (('AP242_MANAGED_MODEL_BASED_3D_ENGINEERING_MIM_LF { 1 0 10303 442 3 1 4 }'));
ENDSEC;

DATA;
#60=COLOUR_RGB('', 0.66274510, 0.83137255, 0.94901961);
#214=SHAPE_REPRESENTATION_RELATIONSHIP('','',#13788,#241);
#241=ADVANCED_BREP_SHAPE_REPRESENTATION('',(#13732),#45478);
#751=CIRCLE('',#14652,0.0123);
#752=CIRCLE('',#14653,0.0188);
#753=CIRCLE('',#14655,0.0123);
#754=CIRCLE('',#14656,0.0188);
#1394=PLANE('',#14651);
#1395=PLANE('',#14654);
#1691=CYLINDRICAL_SURFACE('',#14657,0.0188);
#1692=CYLINDRICAL_SURFACE('',#14658,0.0123);
#4008=ORIENTED_EDGE('',*,*,#6651,.T.);
#4009=ORIENTED_EDGE('',*,*,#6652,.F.);
#4010=ORIENTED_EDGE('',*,*,#6653,.F.);
#4011=ORIENTED_EDGE('',*,*,#6654,.T.);
#4012=ORIENTED_EDGE('',*,*,#6652,.T.);
#4013=ORIENTED_EDGE('',*,*,#6654,.F.);
#4014=ORIENTED_EDGE('',*,*,#6651,.F.);
#4015=ORIENTED_EDGE('',*,*,#6653,.T.);
#6651=EDGE_CURVE('',#8188,#8188,#751,.T.);
#6652=EDGE_CURVE('',#8189,#8189,#752,.T.);
#6653=EDGE_CURVE('',#8190,#8190,#753,.T.);
#6654=EDGE_CURVE('',#8191,#8191,#754,.T.);
#8188=VERTEX_POINT('',#34971);
#8189=VERTEX_POINT('',#34973);
#8190=VERTEX_POINT('',#34976);
#8191=VERTEX_POINT('',#34978);
#11064=EDGE_LOOP('',(#4008));
#11065=EDGE_LOOP('',(#4009));
#11066=EDGE_LOOP('',(#4010));
#11067=EDGE_LOOP('',(#4011));
#11068=EDGE_LOOP('',(#4012));
#11069=EDGE_LOOP('',(#4013));
#11070=EDGE_LOOP('',(#4014));
#11071=EDGE_LOOP('',(#4015));
#12181=FACE_BOUND('',#11064,.T.);
#12182=FACE_BOUND('',#11065,.T.);
#12183=FACE_BOUND('',#11066,.T.);
#12184=FACE_BOUND('',#11067,.T.);
#12185=FACE_BOUND('',#11068,.T.);
#12186=FACE_BOUND('',#11069,.T.);
#12187=FACE_BOUND('',#11070,.T.);
#12188=FACE_BOUND('',#11071,.T.);
#13163=ADVANCED_FACE('',(#12181,#12182),#1394,.F.);
#13164=ADVANCED_FACE('',(#12183,#12184),#1395,.T.);
#13165=ADVANCED_FACE('',(#12185,#12186),#1691,.T.);
#13166=ADVANCED_FACE('',(#12187,#12188),#1692,.F.);
#13515=CLOSED_SHELL('',(#13163,#13164,#13165,#13166));
#13542=STYLED_ITEM('',(#13569),#13732);
#13569=PRESENTATION_STYLE_ASSIGNMENT((#13596));
#13596=SURFACE_STYLE_USAGE(.BOTH.,#13623);
#13623=SURFACE_SIDE_STYLE('',(#13650));
#13650=SURFACE_STYLE_FILL_AREA(#13677);
#13677=FILL_AREA_STYLE('',(#13704));
#13704=FILL_AREA_STYLE_COLOUR('',#60);
#13732=MANIFOLD_SOLID_BREP('Neck_flat_seal',#13515);
#13760=SHAPE_DEFINITION_REPRESENTATION(#45552,#13788);
#13788=SHAPE_REPRESENTATION('Neck_flat_seal',(#13802),#45478);
#13802=AXIS2_PLACEMENT_3D('',#19109,#15295,#15296);
#14651=AXIS2_PLACEMENT_3D('',#34969,#17467,#17468);
#14652=AXIS2_PLACEMENT_3D('',#34970,#17469,#17470);
#14653=AXIS2_PLACEMENT_3D('',#34972,#17471,#17472);
#14654=AXIS2_PLACEMENT_3D('',#34974,#17473,#17474);
#14655=AXIS2_PLACEMENT_3D('',#34975,#17475,#17476);
#14656=AXIS2_PLACEMENT_3D('',#34977,#17477,#17478);
#14657=AXIS2_PLACEMENT_3D('',#34979,#17479,#17480);
#14658=AXIS2_PLACEMENT_3D('',#34980,#17481,#17482);
#15295=DIRECTION('',(0.,0.,1.));
#15296=DIRECTION('',(1.,0.,0.));
#17467=DIRECTION('',(0.,0.,1.));
#17468=DIRECTION('',(1.,0.,0.));
#17469=DIRECTION('',(0.,0.,1.));
#17470=DIRECTION('',(1.,0.,0.));
#17471=DIRECTION('',(0.,0.,1.));
#17472=DIRECTION('',(1.,0.,0.));
#17473=DIRECTION('',(0.,0.,1.));
#17474=DIRECTION('',(1.,0.,0.));
#17475=DIRECTION('',(0.,0.,1.));
#17476=DIRECTION('',(1.,0.,0.));
#17477=DIRECTION('',(0.,0.,1.));
#17478=DIRECTION('',(1.,0.,0.));
#17479=DIRECTION('',(0.,0.,-1.));
#17480=DIRECTION('',(-1.,0.,0.));
#17481=DIRECTION('',(0.,0.,-1.));
#17482=DIRECTION('',(-1.,0.,0.));
#19109=CARTESIAN_POINT('',(0.,0.,0.));
#34969=CARTESIAN_POINT('',(0.,0.,0.046));
#34970=CARTESIAN_POINT('',(0.,0.,0.046));
#34971=CARTESIAN_POINT('',(0.0123,0.,0.046));
#34972=CARTESIAN_POINT('',(0.,0.,0.046));
#34973=CARTESIAN_POINT('',(0.0188,0.,0.046));
#34974=CARTESIAN_POINT('',(0.,0.,0.0469));
#34975=CARTESIAN_POINT('',(0.,0.,0.0469));
#34976=CARTESIAN_POINT('',(0.0123,0.,0.0469));
#34977=CARTESIAN_POINT('',(0.,0.,0.0469));
#34978=CARTESIAN_POINT('',(0.0188,0.,0.0469));
#34979=CARTESIAN_POINT('',(0.,0.,0.0469));
#34980=CARTESIAN_POINT('',(0.,0.,0.0469));
#45463=MECHANICAL_DESIGN_GEOMETRIC_PRESENTATION_REPRESENTATION('',(#13542),#45464);
#45464=(
GEOMETRIC_REPRESENTATION_CONTEXT(3)
GLOBAL_UNCERTAINTY_ASSIGNED_CONTEXT((#45492))
GLOBAL_UNIT_ASSIGNED_CONTEXT((#45522,#45521,#45520))
REPRESENTATION_CONTEXT('MAS-690','TOP_LEVEL_ASSEMBLY_PART')
);
#45478=(
GEOMETRIC_REPRESENTATION_CONTEXT(3)
GLOBAL_UNCERTAINTY_ASSIGNED_CONTEXT((#45506))
GLOBAL_UNIT_ASSIGNED_CONTEXT((#45522,#45521,#45520))
REPRESENTATION_CONTEXT('Neck_flat_seal','COMPONENT_PART')
);
#45492=UNCERTAINTY_MEASURE_WITH_UNIT(LENGTH_MEASURE(1.E-8),#45522,
'DISTANCE_ACCURACY_VALUE','Maximum Tolerance applied to model');
#45506=UNCERTAINTY_MEASURE_WITH_UNIT(LENGTH_MEASURE(1.E-8),#45522,
'DISTANCE_ACCURACY_VALUE','Maximum Tolerance applied to model');
#45520=(
NAMED_UNIT(*)
SI_UNIT($,.STERADIAN.)
SOLID_ANGLE_UNIT()
);
#45521=(
NAMED_UNIT(*)
PLANE_ANGLE_UNIT()
SI_UNIT($,.RADIAN.)
);
#45522=(
LENGTH_UNIT()
NAMED_UNIT(*)
SI_UNIT($,.METRE.)
);
#45552=PRODUCT_DEFINITION_SHAPE('','',#45599);
#45599=PRODUCT_DEFINITION('','',#45655,#45627);
#45627=PRODUCT_DEFINITION_CONTEXT('',#45782,'design');
#45655=PRODUCT_DEFINITION_FORMATION_WITH_SPECIFIED_SOURCE('','',#45711,
 .NOT_KNOWN.);
#45711=PRODUCT('Neck_flat_seal','Neck_flat_seal','Neck_flat_seal',(#45767));
#45767=PRODUCT_CONTEXT('',#45782,'mechanical');
#45782=APPLICATION_CONTEXT('managed model based 3d engineering');
ENDSEC;
END-ISO-10303-21;
